ISO-10303-21;
HEADER;
/* Generated by software containing ST-Developer
 * from STEP Tools, Inc. (www.steptools.com) 
 */

FILE_DESCRIPTION(
/* description */ ('Double-row support with tensioned shaft'),
/* implementation_level */ '2;1');

FILE_NAME(
/* name */ 'Cap Screw - M8x30.step',
/* time_stamp */ '2026-10-27T10:50:35-07:00',
/* author */ (''),
/* organization */ (''),
/* preprocessor_version */ 'ST-DEVELOPER v20.2',
/* originating_system */ 'Autodesk Translation Framework v15.17.0.0',
/* authorisation */ '');

FILE_SCHEMA (('AUTOMOTIVE_DESIGN { 1 0 10303 214 3 1 1 }'));
ENDSEC;

DATA;
#10=MECHANICAL_DESIGN_GEOMETRIC_PRESENTATION_REPRESENTATION('',(#501),#11559);
#399=CONICAL_SURFACE('',#7110,0.625,0.785398163397448);
#400=CONICAL_SURFACE('',#7114,0.635,0.785398163397449);
#401=CONICAL_SURFACE('',#7118,0.41,0.463647609000806);
#402=CONICAL_SURFACE('',#7122,0.36,0.785398163397448);
#409=ORIENTED_CLOSED_SHELL('',*,#6349,.F.);
#412=BREP_WITH_VOIDS('Body1',#6348,(#409));
#436=SHAPE_REPRESENTATION_RELATIONSHIP('SRR','None',#11745,#468);
#468=ADVANCED_BREP_SHAPE_REPRESENTATION('',(#412),#11547);
#501=STYLED_ITEM('',(#11974),#412);
#648=FACE_BOUND('',#1606,.T.);
#839=PLANE('',#7108);
#840=PLANE('',#7116);
#841=PLANE('',#7124);
#842=PLANE('',#7125);
#843=PLANE('',#7126);
#844=PLANE('',#7127);
#845=PLANE('',#7128);
#846=PLANE('',#7129);
#847=PLANE('',#7130);
#848=PLANE('',#7131);
#849=PLANE('',#7132);
#1151=FACE_OUTER_BOUND('',#1601,.T.);
#1152=FACE_OUTER_BOUND('',#1602,.T.);
#1153=FACE_OUTER_BOUND('',#1603,.T.);
#1154=FACE_OUTER_BOUND('',#1604,.T.);
#1155=FACE_OUTER_BOUND('',#1605,.T.);
#1156=FACE_OUTER_BOUND('',#1607,.T.);
#1157=FACE_OUTER_BOUND('',#1608,.T.);
#1158=FACE_OUTER_BOUND('',#1609,.T.);
#1159=FACE_OUTER_BOUND('',#1610,.T.);
#1160=FACE_OUTER_BOUND('',#1611,.T.);
#1161=FACE_OUTER_BOUND('',#1612,.T.);
#1162=FACE_OUTER_BOUND('',#1613,.T.);
#1163=FACE_OUTER_BOUND('',#1614,.T.);
#1164=FACE_OUTER_BOUND('',#1615,.T.);
#1165=FACE_OUTER_BOUND('',#1616,.T.);
#1166=FACE_OUTER_BOUND('',#1617,.T.);
#1167=FACE_OUTER_BOUND('',#1618,.T.);
#1601=EDGE_LOOP('',(#5430));
#1602=EDGE_LOOP('',(#5431,#5432,#5433,#5434));
#1603=EDGE_LOOP('',(#5435,#5436,#5437,#5438));
#1604=EDGE_LOOP('',(#5439,#5440,#5441,#5442));
#1605=EDGE_LOOP('',(#5443));
#1606=EDGE_LOOP('',(#5444));
#1607=EDGE_LOOP('',(#5445,#5446,#5447,#5448));
#1608=EDGE_LOOP('',(#5449,#5450,#5451,#5452));
#1609=EDGE_LOOP('',(#5453,#5454,#5455,#5456));
#1610=EDGE_LOOP('',(#5457));
#1611=EDGE_LOOP('',(#5458,#5459,#5460,#5461));
#1612=EDGE_LOOP('',(#5462,#5463,#5464,#5465));
#1613=EDGE_LOOP('',(#5466,#5467,#5468,#5469));
#1614=EDGE_LOOP('',(#5470,#5471,#5472,#5473));
#1615=EDGE_LOOP('',(#5474,#5475,#5476,#5477));
#1616=EDGE_LOOP('',(#5478,#5479,#5480,#5481));
#1617=EDGE_LOOP('',(#5482,#5483,#5484,#5485,#5486,#5487));
#1618=EDGE_LOOP('',(#5488,#5489,#5490,#5491,#5492,#5493));
#2134=LINE('',#10831,#2681);
#2135=LINE('',#10835,#2682);
#2136=LINE('',#10839,#2683);
#2137=LINE('',#10846,#2684);
#2138=LINE('',#10850,#2685);
#2139=LINE('',#10854,#2686);
#2140=LINE('',#10859,#2687);
#2141=LINE('',#10861,#2688);
#2142=LINE('',#10863,#2689);
#2143=LINE('',#10864,#2690);
#2144=LINE('',#10867,#2691);
#2145=LINE('',#10869,#2692);
#2146=LINE('',#10870,#2693);
#2147=LINE('',#10873,#2694);
#2148=LINE('',#10875,#2695);
#2149=LINE('',#10876,#2696);
#2150=LINE('',#10879,#2697);
#2151=LINE('',#10881,#2698);
#2152=LINE('',#10882,#2699);
#2153=LINE('',#10885,#2700);
#2154=LINE('',#10887,#2701);
#2155=LINE('',#10888,#2702);
#2156=LINE('',#10890,#2703);
#2157=LINE('',#10891,#2704);
#2681=VECTOR('',#8561,0.625);
#2682=VECTOR('',#8566,0.65);
#2683=VECTOR('',#8571,0.635);
#2684=VECTOR('',#8580,0.41);
#2685=VECTOR('',#8585,0.4);
#2686=VECTOR('',#8590,0.36);
#2687=VECTOR('',#8595,1.);
#2688=VECTOR('',#8596,1.);
#2689=VECTOR('',#8597,1.);
#2690=VECTOR('',#8598,1.);
#2691=VECTOR('',#8601,1.);
#2692=VECTOR('',#8602,1.);
#2693=VECTOR('',#8603,1.);
#2694=VECTOR('',#8606,1.);
#2695=VECTOR('',#8607,1.);
#2696=VECTOR('',#8608,1.);
#2697=VECTOR('',#8611,1.);
#2698=VECTOR('',#8612,1.);
#2699=VECTOR('',#8613,1.);
#2700=VECTOR('',#8616,1.);
#2701=VECTOR('',#8617,1.);
#2702=VECTOR('',#8618,1.);
#2703=VECTOR('',#8621,1.);
#2704=VECTOR('',#8622,1.);
#2968=CIRCLE('',#7109,0.6);
#2969=CIRCLE('',#7111,0.65);
#2970=CIRCLE('',#7113,0.65);
#2971=CIRCLE('',#7115,0.62);
#2972=CIRCLE('',#7117,0.42);
#2973=CIRCLE('',#7119,0.3933);
#2974=CIRCLE('',#7121,0.3933);
#2975=CIRCLE('',#7123,0.32);
#3399=VERTEX_POINT('',#10826);
#3400=VERTEX_POINT('',#10829);
#3401=VERTEX_POINT('',#10833);
#3402=VERTEX_POINT('',#10837);
#3403=VERTEX_POINT('',#10841);
#3404=VERTEX_POINT('',#10844);
#3405=VERTEX_POINT('',#10848);
#3406=VERTEX_POINT('',#10852);
#3407=VERTEX_POINT('',#10857);
#3408=VERTEX_POINT('',#10858);
#3409=VERTEX_POINT('',#10860);
#3410=VERTEX_POINT('',#10862);
#3411=VERTEX_POINT('',#10866);
#3412=VERTEX_POINT('',#10868);
#3413=VERTEX_POINT('',#10872);
#3414=VERTEX_POINT('',#10874);
#3415=VERTEX_POINT('',#10878);
#3416=VERTEX_POINT('',#10880);
#3417=VERTEX_POINT('',#10884);
#3418=VERTEX_POINT('',#10886);
#4100=EDGE_CURVE('',#3399,#3399,#2968,.T.);
#4101=EDGE_CURVE('',#3400,#3400,#2969,.T.);
#4102=EDGE_CURVE('',#3400,#3399,#2134,.T.);
#4103=EDGE_CURVE('',#3401,#3401,#2970,.T.);
#4104=EDGE_CURVE('',#3401,#3400,#2135,.T.);
#4105=EDGE_CURVE('',#3402,#3402,#2971,.T.);
#4106=EDGE_CURVE('',#3402,#3401,#2136,.T.);
#4107=EDGE_CURVE('',#3403,#3403,#2972,.T.);
#4108=EDGE_CURVE('',#3404,#3404,#2973,.F.);
#4109=EDGE_CURVE('',#3404,#3403,#2137,.T.);
#4110=EDGE_CURVE('',#3405,#3405,#2974,.F.);
#4111=EDGE_CURVE('',#3405,#3404,#2138,.T.);
#4112=EDGE_CURVE('',#3406,#3406,#2975,.T.);
#4113=EDGE_CURVE('',#3406,#3405,#2139,.T.);
#4114=EDGE_CURVE('',#3407,#3408,#2140,.T.);
#4115=EDGE_CURVE('',#3408,#3409,#2141,.T.);
#4116=EDGE_CURVE('',#3409,#3410,#2142,.T.);
#4117=EDGE_CURVE('',#3407,#3410,#2143,.T.);
#4118=EDGE_CURVE('',#3408,#3411,#2144,.T.);
#4119=EDGE_CURVE('',#3411,#3412,#2145,.T.);
#4120=EDGE_CURVE('',#3412,#3409,#2146,.T.);
#4121=EDGE_CURVE('',#3411,#3413,#2147,.T.);
#4122=EDGE_CURVE('',#3413,#3414,#2148,.T.);
#4123=EDGE_CURVE('',#3414,#3412,#2149,.T.);
#4124=EDGE_CURVE('',#3413,#3415,#2150,.T.);
#4125=EDGE_CURVE('',#3415,#3416,#2151,.T.);
#4126=EDGE_CURVE('',#3416,#3414,#2152,.T.);
#4127=EDGE_CURVE('',#3415,#3417,#2153,.T.);
#4128=EDGE_CURVE('',#3417,#3418,#2154,.T.);
#4129=EDGE_CURVE('',#3418,#3416,#2155,.T.);
#4130=EDGE_CURVE('',#3417,#3407,#2156,.T.);
#4131=EDGE_CURVE('',#3410,#3418,#2157,.T.);
#5430=ORIENTED_EDGE('',*,*,#4100,.F.);
#5431=ORIENTED_EDGE('',*,*,#4101,.F.);
#5432=ORIENTED_EDGE('',*,*,#4102,.T.);
#5433=ORIENTED_EDGE('',*,*,#4100,.T.);
#5434=ORIENTED_EDGE('',*,*,#4102,.F.);
#5435=ORIENTED_EDGE('',*,*,#4103,.F.);
#5436=ORIENTED_EDGE('',*,*,#4104,.T.);
#5437=ORIENTED_EDGE('',*,*,#4101,.T.);
#5438=ORIENTED_EDGE('',*,*,#4104,.F.);
#5439=ORIENTED_EDGE('',*,*,#4105,.F.);
#5440=ORIENTED_EDGE('',*,*,#4106,.T.);
#5441=ORIENTED_EDGE('',*,*,#4103,.T.);
#5442=ORIENTED_EDGE('',*,*,#4106,.F.);
#5443=ORIENTED_EDGE('',*,*,#4105,.T.);
#5444=ORIENTED_EDGE('',*,*,#4107,.F.);
#5445=ORIENTED_EDGE('',*,*,#4108,.F.);
#5446=ORIENTED_EDGE('',*,*,#4109,.T.);
#5447=ORIENTED_EDGE('',*,*,#4107,.T.);
#5448=ORIENTED_EDGE('',*,*,#4109,.F.);
#5449=ORIENTED_EDGE('',*,*,#4110,.F.);
#5450=ORIENTED_EDGE('',*,*,#4111,.T.);
#5451=ORIENTED_EDGE('',*,*,#4108,.T.);
#5452=ORIENTED_EDGE('',*,*,#4111,.F.);
#5453=ORIENTED_EDGE('',*,*,#4112,.F.);
#5454=ORIENTED_EDGE('',*,*,#4113,.T.);
#5455=ORIENTED_EDGE('',*,*,#4110,.T.);
#5456=ORIENTED_EDGE('',*,*,#4113,.F.);
#5457=ORIENTED_EDGE('',*,*,#4112,.T.);
#5458=ORIENTED_EDGE('',*,*,#4114,.T.);
#5459=ORIENTED_EDGE('',*,*,#4115,.T.);
#5460=ORIENTED_EDGE('',*,*,#4116,.T.);
#5461=ORIENTED_EDGE('',*,*,#4117,.F.);
#5462=ORIENTED_EDGE('',*,*,#4118,.T.);
#5463=ORIENTED_EDGE('',*,*,#4119,.T.);
#5464=ORIENTED_EDGE('',*,*,#4120,.T.);
#5465=ORIENTED_EDGE('',*,*,#4115,.F.);
#5466=ORIENTED_EDGE('',*,*,#4121,.T.);
#5467=ORIENTED_EDGE('',*,*,#4122,.T.);
#5468=ORIENTED_EDGE('',*,*,#4123,.T.);
#5469=ORIENTED_EDGE('',*,*,#4119,.F.);
#5470=ORIENTED_EDGE('',*,*,#4124,.T.);
#5471=ORIENTED_EDGE('',*,*,#4125,.T.);
#5472=ORIENTED_EDGE('',*,*,#4126,.T.);
#5473=ORIENTED_EDGE('',*,*,#4122,.F.);
#5474=ORIENTED_EDGE('',*,*,#4127,.T.);
#5475=ORIENTED_EDGE('',*,*,#4128,.T.);
#5476=ORIENTED_EDGE('',*,*,#4129,.T.);
#5477=ORIENTED_EDGE('',*,*,#4125,.F.);
#5478=ORIENTED_EDGE('',*,*,#4130,.T.);
#5479=ORIENTED_EDGE('',*,*,#4117,.T.);
#5480=ORIENTED_EDGE('',*,*,#4131,.T.);
#5481=ORIENTED_EDGE('',*,*,#4128,.F.);
#5482=ORIENTED_EDGE('',*,*,#4130,.F.);
#5483=ORIENTED_EDGE('',*,*,#4127,.F.);
#5484=ORIENTED_EDGE('',*,*,#4124,.F.);
#5485=ORIENTED_EDGE('',*,*,#4121,.F.);
#5486=ORIENTED_EDGE('',*,*,#4118,.F.);
#5487=ORIENTED_EDGE('',*,*,#4114,.F.);
#5488=ORIENTED_EDGE('',*,*,#4131,.F.);
#5489=ORIENTED_EDGE('',*,*,#4116,.F.);
#5490=ORIENTED_EDGE('',*,*,#4120,.F.);
#5491=ORIENTED_EDGE('',*,*,#4123,.F.);
#5492=ORIENTED_EDGE('',*,*,#4126,.F.);
#5493=ORIENTED_EDGE('',*,*,#4129,.F.);
#5956=CYLINDRICAL_SURFACE('',#7112,0.65);
#5957=CYLINDRICAL_SURFACE('',#7120,0.3933);
#6214=ADVANCED_FACE('',(#1151),#839,.T.);
#6215=ADVANCED_FACE('',(#1152),#399,.T.);
#6216=ADVANCED_FACE('',(#1153),#5956,.T.);
#6217=ADVANCED_FACE('',(#1154),#400,.T.);
#6218=ADVANCED_FACE('',(#1155,#648),#840,.T.);
#6219=ADVANCED_FACE('',(#1156),#401,.T.);
#6220=ADVANCED_FACE('',(#1157),#5957,.T.);
#6221=ADVANCED_FACE('',(#1158),#402,.T.);
#6222=ADVANCED_FACE('',(#1159),#841,.T.);
#6223=ADVANCED_FACE('',(#1160),#842,.F.);
#6224=ADVANCED_FACE('',(#1161),#843,.F.);
#6225=ADVANCED_FACE('',(#1162),#844,.F.);
#6226=ADVANCED_FACE('',(#1163),#845,.F.);
#6227=ADVANCED_FACE('',(#1164),#846,.F.);
#6228=ADVANCED_FACE('',(#1165),#847,.F.);
#6229=ADVANCED_FACE('',(#1166),#848,.F.);
#6230=ADVANCED_FACE('',(#1167),#849,.F.);
#6348=CLOSED_SHELL('',(#6214,#6215,#6216,#6217,#6218,#6219,#6220,#6221,
#6222));
#6349=CLOSED_SHELL('',(#6223,#6224,#6225,#6226,#6227,#6228,#6229,#6230));
#7107=AXIS2_PLACEMENT_3D('',#10824,#8551,#8552);
#7108=AXIS2_PLACEMENT_3D('',#10825,#8553,#8554);
#7109=AXIS2_PLACEMENT_3D('',#10827,#8555,#8556);
#7110=AXIS2_PLACEMENT_3D('',#10828,#8557,#8558);
#7111=AXIS2_PLACEMENT_3D('',#10830,#8559,#8560);
#7112=AXIS2_PLACEMENT_3D('',#10832,#8562,#8563);
#7113=AXIS2_PLACEMENT_3D('',#10834,#8564,#8565);
#7114=AXIS2_PLACEMENT_3D('',#10836,#8567,#8568);
#7115=AXIS2_PLACEMENT_3D('',#10838,#8569,#8570);
#7116=AXIS2_PLACEMENT_3D('',#10840,#8572,#8573);
#7117=AXIS2_PLACEMENT_3D('',#10842,#8574,#8575);
#7118=AXIS2_PLACEMENT_3D('',#10843,#8576,#8577);
#7119=AXIS2_PLACEMENT_3D('',#10845,#8578,#8579);
#7120=AXIS2_PLACEMENT_3D('',#10847,#8581,#8582);
#7121=AXIS2_PLACEMENT_3D('',#10849,#8583,#8584);
#7122=AXIS2_PLACEMENT_3D('',#10851,#8586,#8587);
#7123=AXIS2_PLACEMENT_3D('',#10853,#8588,#8589);
#7124=AXIS2_PLACEMENT_3D('',#10855,#8591,#8592);
#7125=AXIS2_PLACEMENT_3D('',#10856,#8593,#8594);
#7126=AXIS2_PLACEMENT_3D('',#10865,#8599,#8600);
#7127=AXIS2_PLACEMENT_3D('',#10871,#8604,#8605);
#7128=AXIS2_PLACEMENT_3D('',#10877,#8609,#8610);
#7129=AXIS2_PLACEMENT_3D('',#10883,#8614,#8615);
#7130=AXIS2_PLACEMENT_3D('',#10889,#8619,#8620);
#7131=AXIS2_PLACEMENT_3D('',#10892,#8623,#8624);
#7132=AXIS2_PLACEMENT_3D('',#10893,#8625,#8626);
#8551=DIRECTION('axis',(0.,0.,1.));
#8552=DIRECTION('refdir',(1.,0.,0.));
#8553=DIRECTION('center_axis',(0.,1.,0.));
#8554=DIRECTION('ref_axis',(0.,0.,1.));
#8555=DIRECTION('center_axis',(0.,-1.,0.));
#8556=DIRECTION('ref_axis',(1.,0.,0.));
#8557=DIRECTION('center_axis',(0.,-1.,0.));
#8558=DIRECTION('ref_axis',(1.,0.,0.));
#8559=DIRECTION('center_axis',(0.,-1.,0.));
#8560=DIRECTION('ref_axis',(1.,0.,0.));
#8561=DIRECTION('',(0.707106781186548,0.707106781186547,8.65956056235493E-17));
#8562=DIRECTION('center_axis',(0.,-1.,0.));
#8563=DIRECTION('ref_axis',(1.,0.,0.));
#8564=DIRECTION('center_axis',(0.,-1.,0.));
#8565=DIRECTION('ref_axis',(1.,0.,0.));
#8566=DIRECTION('',(0.,1.,0.));
#8567=DIRECTION('center_axis',(0.,1.,0.));
#8568=DIRECTION('ref_axis',(1.,0.,0.));
#8569=DIRECTION('center_axis',(0.,-1.,0.));
#8570=DIRECTION('ref_axis',(1.,0.,0.));
#8571=DIRECTION('',(-0.707106781186548,0.707106781186547,-8.65956056235494E-17));
#8572=DIRECTION('center_axis',(0.,-1.,0.));
#8573=DIRECTION('ref_axis',(0.,0.,-1.));
#8574=DIRECTION('center_axis',(0.,-1.,0.));
#8575=DIRECTION('ref_axis',(1.,0.,0.));
#8576=DIRECTION('center_axis',(0.,1.,0.));
#8577=DIRECTION('ref_axis',(1.,0.,0.));
#8578=DIRECTION('center_axis',(0.,1.,0.));
#8579=DIRECTION('ref_axis',(1.,0.,0.));
#8580=DIRECTION('',(-0.447213595499958,0.894427190999916,-5.47678698264203E-17));
#8581=DIRECTION('center_axis',(0.,-1.,0.));
#8582=DIRECTION('ref_axis',(1.,0.,0.));
#8583=DIRECTION('center_axis',(0.,1.,0.));
#8584=DIRECTION('ref_axis',(1.,0.,0.));
#8585=DIRECTION('',(0.,1.,0.));
#8586=DIRECTION('center_axis',(0.,1.,0.));
#8587=DIRECTION('ref_axis',(1.,0.,0.));
#8588=DIRECTION('center_axis',(0.,-1.,0.));
#8589=DIRECTION('ref_axis',(1.,0.,0.));
#8590=DIRECTION('',(-0.707106781186547,0.707106781186548,-8.65956056235493E-17));
#8591=DIRECTION('center_axis',(0.,-1.,0.));
#8592=DIRECTION('ref_axis',(0.,0.,-1.));
#8593=DIRECTION('center_axis',(0.866025403784439,0.,-0.5));
#8594=DIRECTION('ref_axis',(0.5,0.,0.866025403784439));
#8595=DIRECTION('',(-0.5,0.,-0.866025403784439));
#8596=DIRECTION('',(0.,-1.,0.));
#8597=DIRECTION('',(0.5,0.,0.866025403784439));
#8598=DIRECTION('',(0.,-1.,0.));
#8599=DIRECTION('center_axis',(1.60246890531964E-16,0.,-1.));
#8600=DIRECTION('ref_axis',(1.,0.,1.60246890531964E-16));
#8601=DIRECTION('',(-1.,0.,-1.60246890531964E-16));
#8602=DIRECTION('',(0.,-1.,0.));
#8603=DIRECTION('',(1.,0.,1.60246890531964E-16));
#8604=DIRECTION('center_axis',(-0.866025403784439,0.,-0.5));
#8605=DIRECTION('ref_axis',(0.5,0.,-0.866025403784439));
#8606=DIRECTION('',(-0.5,0.,0.866025403784439));
#8607=DIRECTION('',(0.,-1.,0.));
#8608=DIRECTION('',(0.5,0.,-0.866025403784439));
#8609=DIRECTION('center_axis',(-0.866025403784439,0.,0.5));
#8610=DIRECTION('ref_axis',(-0.5,0.,-0.866025403784439));
#8611=DIRECTION('',(0.5,0.,0.866025403784439));
#8612=DIRECTION('',(0.,-1.,0.));
#8613=DIRECTION('',(-0.5,0.,-0.866025403784439));
#8614=DIRECTION('center_axis',(-1.60246890531964E-16,0.,1.));
#8615=DIRECTION('ref_axis',(-1.,0.,-1.60246890531964E-16));
#8616=DIRECTION('',(1.,0.,1.60246890531964E-16));
#8617=DIRECTION('',(0.,-1.,0.));
#8618=DIRECTION('',(-1.,0.,-1.60246890531964E-16));
#8619=DIRECTION('center_axis',(0.866025403784439,0.,0.5));
#8620=DIRECTION('ref_axis',(-0.5,0.,0.866025403784439));
#8621=DIRECTION('',(0.5,0.,-0.866025403784439));
#8622=DIRECTION('',(-0.5,0.,0.866025403784439));
#8623=DIRECTION('center_axis',(0.,1.,0.));
#8624=DIRECTION('ref_axis',(1.,0.,0.));
#8625=DIRECTION('center_axis',(0.,-1.,0.));
#8626=DIRECTION('ref_axis',(0.,0.,-1.));
#10824=CARTESIAN_POINT('',(0.,0.,0.));
#10825=CARTESIAN_POINT('Origin',(0.6,0.8,0.));
#10826=CARTESIAN_POINT('',(-0.6,0.8,-7.34788079488412E-17));
#10827=CARTESIAN_POINT('Origin',(0.,0.8,0.));
#10828=CARTESIAN_POINT('Origin',(0.,0.775,0.));
#10829=CARTESIAN_POINT('',(-0.65,0.75,-7.9602041944578E-17));
#10830=CARTESIAN_POINT('Origin',(0.,0.75,0.));
#10831=CARTESIAN_POINT('',(-0.625,0.775,-7.65404249467096E-17));
#10832=CARTESIAN_POINT('Origin',(0.,0.39,0.));
#10833=CARTESIAN_POINT('',(-0.65,0.0299999999999998,-7.9602041944578E-17));
#10834=CARTESIAN_POINT('Origin',(0.,0.0299999999999998,0.));
#10835=CARTESIAN_POINT('',(-0.65,0.39,-7.9602041944578E-17));
#10836=CARTESIAN_POINT('Origin',(0.,0.0150000000000001,0.));
#10837=CARTESIAN_POINT('',(-0.62,5.89805981832114E-17,-7.59281015471359E-17));
#10838=CARTESIAN_POINT('Origin',(0.,0.,0.));
#10839=CARTESIAN_POINT('',(-0.635,0.0150000000000001,-7.77650717458569E-17));
#10840=CARTESIAN_POINT('Origin',(0.42,0.,0.));
#10841=CARTESIAN_POINT('',(-0.42,-3.46944695195361E-18,-5.14351655641888E-17));
#10842=CARTESIAN_POINT('Origin',(0.,0.,0.));
#10843=CARTESIAN_POINT('Origin',(0.,-0.02,0.));
#10844=CARTESIAN_POINT('',(-0.3933,-0.0534000000000001,4.81653586104654E-17));
#10845=CARTESIAN_POINT('Origin',(0.,-0.0534000000000001,0.));
#10846=CARTESIAN_POINT('',(-0.41,-0.02,-5.02105187650415E-17));
#10847=CARTESIAN_POINT('Origin',(0.,-1.48,0.));
#10848=CARTESIAN_POINT('',(-0.3933,-2.9267,4.81653586104654E-17));
#10849=CARTESIAN_POINT('Origin',(0.,-2.9267,0.));
#10850=CARTESIAN_POINT('',(-0.3933,-1.48,-4.81653586104654E-17));
#10851=CARTESIAN_POINT('Origin',(0.,-2.96,0.));
#10852=CARTESIAN_POINT('',(-0.32,-3.,-3.91886975727153E-17));
#10853=CARTESIAN_POINT('Origin',(0.,-3.,0.));
#10854=CARTESIAN_POINT('',(-0.36,-2.96,-4.40872847693047E-17));
#10855=CARTESIAN_POINT('Origin',(0.,-3.,0.));
#10856=CARTESIAN_POINT('Origin',(0.173205080756888,-0.8,-0.3));
#10857=CARTESIAN_POINT('',(0.346410161513775,-0.8,0.));
#10858=CARTESIAN_POINT('',(0.173205080756888,-0.8,-0.3));
#10859=CARTESIAN_POINT('',(0.346410161513775,-0.8,0.));
#10860=CARTESIAN_POINT('',(0.173205080756888,-1.28,-0.3));
#10861=CARTESIAN_POINT('',(0.173205080756888,-0.8,-0.3));
#10862=CARTESIAN_POINT('',(0.346410161513775,-1.28,0.));
#10863=CARTESIAN_POINT('',(0.346410161513775,-1.28,0.));
#10864=CARTESIAN_POINT('',(0.346410161513775,-0.8,0.));
#10865=CARTESIAN_POINT('Origin',(-0.173205080756888,-0.8,-0.3));
#10866=CARTESIAN_POINT('',(-0.173205080756888,-0.8,-0.3));
#10867=CARTESIAN_POINT('',(0.173205080756888,-0.8,-0.3));
#10868=CARTESIAN_POINT('',(-0.173205080756888,-1.28,-0.3));
#10869=CARTESIAN_POINT('',(-0.173205080756888,-0.8,-0.3));
#10870=CARTESIAN_POINT('',(0.173205080756888,-1.28,-0.3));
#10871=CARTESIAN_POINT('Origin',(-0.346410161513775,-0.8,-5.55111512312578E-17));
#10872=CARTESIAN_POINT('',(-0.346410161513775,-0.8,-4.24230095489963E-17));
#10873=CARTESIAN_POINT('',(-0.173205080756888,-0.8,-0.3));
#10874=CARTESIAN_POINT('',(-0.346410161513775,-1.28,-5.55111512312578E-17));
#10875=CARTESIAN_POINT('',(-0.346410161513775,-0.8,-4.24230095489963E-17));
#10876=CARTESIAN_POINT('',(-0.173205080756888,-1.28,-0.3));
#10877=CARTESIAN_POINT('Origin',(-0.173205080756888,-0.8,0.3));
#10878=CARTESIAN_POINT('',(-0.173205080756888,-0.8,0.3));
#10879=CARTESIAN_POINT('',(-0.346410161513775,-0.8,-4.24230095489963E-17));
#10880=CARTESIAN_POINT('',(-0.173205080756888,-1.28,0.3));
#10881=CARTESIAN_POINT('',(-0.173205080756888,-0.8,0.3));
#10882=CARTESIAN_POINT('',(-0.346410161513775,-1.28,-4.24230095489963E-17));
#10883=CARTESIAN_POINT('Origin',(0.173205080756888,-0.8,0.3));
#10884=CARTESIAN_POINT('',(0.173205080756888,-0.8,0.3));
#10885=CARTESIAN_POINT('',(-0.173205080756888,-0.8,0.3));
#10886=CARTESIAN_POINT('',(0.173205080756888,-1.28,0.3));
#10887=CARTESIAN_POINT('',(0.173205080756888,-0.8,0.3));
#10888=CARTESIAN_POINT('',(-0.173205080756888,-1.28,0.3));
#10889=CARTESIAN_POINT('Origin',(0.346410161513775,-0.8,0.));
#10890=CARTESIAN_POINT('',(0.173205080756888,-0.8,0.3));
#10891=CARTESIAN_POINT('',(0.173205080756888,-1.28,0.3));
#10892=CARTESIAN_POINT('Origin',(0.,-0.8,-5.55111512312578E-17));
#10893=CARTESIAN_POINT('Origin',(0.,-1.28,-5.55111512312578E-17));
#11510=UNCERTAINTY_MEASURE_WITH_UNIT(LENGTH_MEASURE(0.001),#11560,
'DISTANCE_ACCURACY_VALUE',
'Maximum model space distance between geometric entities at asserted c
onnectivities');
#11522=UNCERTAINTY_MEASURE_WITH_UNIT(LENGTH_MEASURE(0.001),#11560,
'DISTANCE_ACCURACY_VALUE',
'Maximum model space distance between geometric entities at asserted c
onnectivities');
#11547=(
GEOMETRIC_REPRESENTATION_CONTEXT(3)
GLOBAL_UNCERTAINTY_ASSIGNED_CONTEXT((#11510))
GLOBAL_UNIT_ASSIGNED_CONTEXT((#11560,#11562,#11563))
REPRESENTATION_CONTEXT('','3D')
);
#11559=(
GEOMETRIC_REPRESENTATION_CONTEXT(3)
GLOBAL_UNCERTAINTY_ASSIGNED_CONTEXT((#11522))
GLOBAL_UNIT_ASSIGNED_CONTEXT((#11560,#11562,#11563))
REPRESENTATION_CONTEXT('','3D')
);
#11560=(
LENGTH_UNIT()
NAMED_UNIT(*)
SI_UNIT(.CENTI.,.METRE.)
);
#11562=(
NAMED_UNIT(*)
PLANE_ANGLE_UNIT()
SI_UNIT($,.RADIAN.)
);
#11563=(
NAMED_UNIT(*)
SI_UNIT($,.STERADIAN.)
SOLID_ANGLE_UNIT()
);
#11588=SHAPE_DEFINITION_REPRESENTATION(#11626,#11745);
#11626=PRODUCT_DEFINITION_SHAPE('',$,#11782);
#11745=SHAPE_REPRESENTATION('',(#7107),#11547);
#11757=PRODUCT_DEFINITION_CONTEXT('part definition',#11867,'design');
#11782=PRODUCT_DEFINITION('Cap Screw - M8x30','Cap Screw - M8x30',#11818,
#11757);
#11818=PRODUCT_DEFINITION_FORMATION('',$,#11893);
#11867=APPLICATION_CONTEXT(
'Core Data for Automotive Mechanical Design Process');
#11868=PRODUCT_CONTEXT('part definition',#11867,'mechanical');
#11893=PRODUCT('Cap Screw - M8x30','Cap Screw - M8x30',
'Cap Screw - M8x30',(#11868));
#11968=COLOUR_RGB('Black',0.12,0.14,0.17);
#11969=FILL_AREA_STYLE_COLOUR('',#11968);
#11970=FILL_AREA_STYLE('',(#11969));
#11971=SURFACE_STYLE_FILL_AREA(#11970);
#11972=SURFACE_SIDE_STYLE('',(#11971));
#11973=SURFACE_STYLE_USAGE(.BOTH.,#11972);
#11974=PRESENTATION_STYLE_ASSIGNMENT((#11973));
ENDSEC;
END-ISO-10303-21;
